ISO-10303-21;
HEADER;
/* Generated by software containing ST-Developer
 * from STEP Tools, Inc. (www.steptools.com) 
 */

FILE_DESCRIPTION(
/* description */ ('STEP AP214'),
/* implementation_level */ '2;1');

FILE_NAME(
/* name */ 'Heavy Hex Bolt 0.625-18 x 1.75 x 1.25.step',
/* time_stamp */ '2026-11-14T07:13:32-08:00',
/* author */ (''),
/* organization */ (''),
/* preprocessor_version */ 'ST-DEVELOPER v20.2',
/* originating_system */ 'Autodesk Translation Framework v15.17.0.0',
/* authorisation */ '');

FILE_SCHEMA (('AUTOMOTIVE_DESIGN { 1 0 10303 214 3 1 1 }'));
ENDSEC;

DATA;
#10=MECHANICAL_DESIGN_GEOMETRIC_PRESENTATION_REPRESENTATION('',(#1319),#32903);
#408=(
BOUNDED_CURVE()
B_SPLINE_CURVE(2,(#22731,#22732,#22733),.UNSPECIFIED.,.F.,.F.)
B_SPLINE_CURVE_WITH_KNOTS((3,3),(2.04583671611078,3.4301435642622),
 .UNSPECIFIED.)
CURVE()
GEOMETRIC_REPRESENTATION_ITEM()
RATIONAL_B_SPLINE_CURVE((1.65994685877124,1.78834419513797,1.78834419513797))
REPRESENTATION_ITEM('')
);
#409=(
BOUNDED_CURVE()
B_SPLINE_CURVE(2,(#22740,#22741,#22742),.UNSPECIFIED.,.F.,.F.)
B_SPLINE_CURVE_WITH_KNOTS((3,3),(3.4301435642622,4.81445041241362),
 .UNSPECIFIED.)
CURVE()
GEOMETRIC_REPRESENTATION_ITEM()
RATIONAL_B_SPLINE_CURVE((1.78834419513797,1.78834419513797,1.65994685877124))
REPRESENTATION_ITEM('')
);
#410=(
BOUNDED_CURVE()
B_SPLINE_CURVE(2,(#22746,#22747,#22748),.UNSPECIFIED.,.F.,.F.)
B_SPLINE_CURVE_WITH_KNOTS((3,3),(2.04583671611078,3.4301435642622),
 .UNSPECIFIED.)
CURVE()
GEOMETRIC_REPRESENTATION_ITEM()
RATIONAL_B_SPLINE_CURVE((1.65994685877124,1.78834419513797,1.78834419513797))
REPRESENTATION_ITEM('')
);
#411=(
BOUNDED_CURVE()
B_SPLINE_CURVE(2,(#22752,#22753,#22754),.UNSPECIFIED.,.F.,.F.)
B_SPLINE_CURVE_WITH_KNOTS((3,3),(3.4301435642622,4.81445041241363),
 .UNSPECIFIED.)
CURVE()
GEOMETRIC_REPRESENTATION_ITEM()
RATIONAL_B_SPLINE_CURVE((1.78834419513797,1.78834419513797,1.65994685877124))
REPRESENTATION_ITEM('')
);
#412=(
BOUNDED_CURVE()
B_SPLINE_CURVE(2,(#22758,#22759,#22760),.UNSPECIFIED.,.F.,.F.)
B_SPLINE_CURVE_WITH_KNOTS((3,3),(2.04583671611078,3.4301435642622),
 .UNSPECIFIED.)
CURVE()
GEOMETRIC_REPRESENTATION_ITEM()
RATIONAL_B_SPLINE_CURVE((1.65994685877124,1.78834419513797,1.78834419513797))
REPRESENTATION_ITEM('')
);
#413=(
BOUNDED_CURVE()
B_SPLINE_CURVE(2,(#22764,#22765,#22766),.UNSPECIFIED.,.F.,.F.)
B_SPLINE_CURVE_WITH_KNOTS((3,3),(3.4301435642622,4.81445041241362),
 .UNSPECIFIED.)
CURVE()
GEOMETRIC_REPRESENTATION_ITEM()
RATIONAL_B_SPLINE_CURVE((1.78834419513797,1.78834419513797,1.65994685877124))
REPRESENTATION_ITEM('')
);
#414=(
BOUNDED_CURVE()
B_SPLINE_CURVE(2,(#22770,#22771,#22772),.UNSPECIFIED.,.F.,.F.)
B_SPLINE_CURVE_WITH_KNOTS((3,3),(2.04583671611077,3.4301435642622),
 .UNSPECIFIED.)
CURVE()
GEOMETRIC_REPRESENTATION_ITEM()
RATIONAL_B_SPLINE_CURVE((1.65994685877124,1.78834419513797,1.78834419513797))
REPRESENTATION_ITEM('')
);
#415=(
BOUNDED_CURVE()
B_SPLINE_CURVE(2,(#22776,#22777,#22778),.UNSPECIFIED.,.F.,.F.)
B_SPLINE_CURVE_WITH_KNOTS((3,3),(3.4301435642622,4.81445041241362),
 .UNSPECIFIED.)
CURVE()
GEOMETRIC_REPRESENTATION_ITEM()
RATIONAL_B_SPLINE_CURVE((1.78834419513797,1.78834419513797,1.65994685877124))
REPRESENTATION_ITEM('')
);
#416=(
BOUNDED_CURVE()
B_SPLINE_CURVE(2,(#22782,#22783,#22784),.UNSPECIFIED.,.F.,.F.)
B_SPLINE_CURVE_WITH_KNOTS((3,3),(2.04583671611079,3.4301435642622),
 .UNSPECIFIED.)
CURVE()
GEOMETRIC_REPRESENTATION_ITEM()
RATIONAL_B_SPLINE_CURVE((1.65994685877123,1.78834419513797,1.78834419513797))
REPRESENTATION_ITEM('')
);
#417=(
BOUNDED_CURVE()
B_SPLINE_CURVE(2,(#22788,#22789,#22790),.UNSPECIFIED.,.F.,.F.)
B_SPLINE_CURVE_WITH_KNOTS((3,3),(3.4301435642622,4.81445041241362),
 .UNSPECIFIED.)
CURVE()
GEOMETRIC_REPRESENTATION_ITEM()
RATIONAL_B_SPLINE_CURVE((1.78834419513797,1.78834419513797,1.65994685877123))
REPRESENTATION_ITEM('')
);
#418=(
BOUNDED_CURVE()
B_SPLINE_CURVE(2,(#22793,#22794,#22795),.UNSPECIFIED.,.F.,.F.)
B_SPLINE_CURVE_WITH_KNOTS((3,3),(2.04583671611079,3.4301435642622),
 .UNSPECIFIED.)
CURVE()
GEOMETRIC_REPRESENTATION_ITEM()
RATIONAL_B_SPLINE_CURVE((1.65994685877124,1.78834419513797,1.78834419513797))
REPRESENTATION_ITEM('')
);
#419=(
BOUNDED_CURVE()
B_SPLINE_CURVE(2,(#22797,#22798,#22799),.UNSPECIFIED.,.F.,.F.)
B_SPLINE_CURVE_WITH_KNOTS((3,3),(3.4301435642622,4.81445041241362),
 .UNSPECIFIED.)
CURVE()
GEOMETRIC_REPRESENTATION_ITEM()
RATIONAL_B_SPLINE_CURVE((1.78834419513797,1.78834419513797,1.65994685877124))
REPRESENTATION_ITEM('')
);
#574=CONICAL_SURFACE('',#16277,7.09803,0.785398163397448);
#575=CONICAL_SURFACE('',#16290,13.4874,1.0471975511966);
#576=CONICAL_SURFACE('',#16292,13.4874,1.0471975511966);
#577=CONICAL_SURFACE('',#16294,13.4874,1.0471975511966);
#578=CONICAL_SURFACE('',#16296,13.4874,1.0471975511966);
#579=CONICAL_SURFACE('',#16298,13.4874,1.0471975511966);
#580=CONICAL_SURFACE('',#16300,13.4874,1.0471975511966);
#676=SHAPE_REPRESENTATION_RELATIONSHIP('SRR','None',#33018,#690);
#690=ADVANCED_BREP_SHAPE_REPRESENTATION('',(#1408),#32893);
#882=CIRCLE('',#16278,7.9375);
#883=CIRCLE('',#16279,7.09803);
#884=CIRCLE('',#16281,7.9375);
#885=CIRCLE('',#16291,13.4874);
#886=CIRCLE('',#16293,13.4874);
#887=CIRCLE('',#16295,13.4874);
#888=CIRCLE('',#16297,13.4874);
#889=CIRCLE('',#16299,13.4874);
#890=CIRCLE('',#16301,13.4874);
#1182=CYLINDRICAL_SURFACE('',#16280,7.9375);
#1319=STYLED_ITEM('',(#33099),#1408);
#1408=MANIFOLD_SOLID_BREP('Body1',#15567);
#1595=FACE_BOUND('',#2987,.T.);
#1957=FACE_OUTER_BOUND('',#2978,.T.);
#1958=FACE_OUTER_BOUND('',#2979,.T.);
#1959=FACE_OUTER_BOUND('',#2980,.T.);
#1960=FACE_OUTER_BOUND('',#2981,.T.);
#1961=FACE_OUTER_BOUND('',#2982,.T.);
#1962=FACE_OUTER_BOUND('',#2983,.T.);
#1963=FACE_OUTER_BOUND('',#2984,.T.);
#1964=FACE_OUTER_BOUND('',#2985,.T.);
#1965=FACE_OUTER_BOUND('',#2986,.T.);
#1966=FACE_OUTER_BOUND('',#2988,.T.);
#1967=FACE_OUTER_BOUND('',#2989,.T.);
#1968=FACE_OUTER_BOUND('',#2990,.T.);
#1969=FACE_OUTER_BOUND('',#2991,.T.);
#1970=FACE_OUTER_BOUND('',#2992,.T.);
#1971=FACE_OUTER_BOUND('',#2993,.T.);
#1972=FACE_OUTER_BOUND('',#2994,.T.);
#1973=FACE_OUTER_BOUND('',#2995,.T.);
#2978=EDGE_LOOP('',(#11253,#11254,#11255,#11256));
#2979=EDGE_LOOP('',(#11257,#11258,#11259,#11260));
#2980=EDGE_LOOP('',(#11261,#11262,#11263,#11264,#11265));
#2981=EDGE_LOOP('',(#11266,#11267,#11268,#11269,#11270));
#2982=EDGE_LOOP('',(#11271,#11272,#11273,#11274,#11275));
#2983=EDGE_LOOP('',(#11276,#11277,#11278,#11279,#11280));
#2984=EDGE_LOOP('',(#11281,#11282,#11283,#11284,#11285));
#2985=EDGE_LOOP('',(#11286,#11287,#11288,#11289,#11290));
#2986=EDGE_LOOP('',(#11291,#11292,#11293,#11294,#11295,#11296));
#2987=EDGE_LOOP('',(#11297));
#2988=EDGE_LOOP('',(#11298));
#2989=EDGE_LOOP('',(#11299,#11300,#11301));
#2990=EDGE_LOOP('',(#11302,#11303,#11304));
#2991=EDGE_LOOP('',(#11305,#11306,#11307));
#2992=EDGE_LOOP('',(#11308,#11309,#11310));
#2993=EDGE_LOOP('',(#11311,#11312,#11313));
#2994=EDGE_LOOP('',(#11314,#11315,#11316));
#2995=EDGE_LOOP('',(#11317,#11318,#11319,#11320,#11321,#11322));
#4140=LINE('',#22722,#5544);
#4141=LINE('',#22727,#5545);
#4142=LINE('',#22735,#5546);
#4143=LINE('',#22737,#5547);
#4144=LINE('',#22739,#5548);
#4145=LINE('',#22750,#5549);
#4146=LINE('',#22751,#5550);
#4147=LINE('',#22762,#5551);
#4148=LINE('',#22763,#5552);
#4149=LINE('',#22774,#5553);
#4150=LINE('',#22775,#5554);
#4151=LINE('',#22786,#5555);
#4152=LINE('',#22787,#5556);
#4153=LINE('',#22796,#5557);
#5544=VECTOR('',#18616,7.09803);
#5545=VECTOR('',#18623,7.9375);
#5546=VECTOR('',#18626,1000.);
#5547=VECTOR('',#18627,1000.);
#5548=VECTOR('',#18628,1000.);
#5549=VECTOR('',#18631,1000.);
#5550=VECTOR('',#18632,1000.);
#5551=VECTOR('',#18635,1000.);
#5552=VECTOR('',#18636,1000.);
#5553=VECTOR('',#18639,1000.);
#5554=VECTOR('',#18640,1000.);
#5555=VECTOR('',#18643,1000.);
#5556=VECTOR('',#18644,1000.);
#5557=VECTOR('',#18647,1000.);
#6929=VERTEX_POINT('',#22719);
#6930=VERTEX_POINT('',#22721);
#6931=VERTEX_POINT('',#22725);
#6932=VERTEX_POINT('',#22729);
#6933=VERTEX_POINT('',#22730);
#6934=VERTEX_POINT('',#22734);
#6935=VERTEX_POINT('',#22736);
#6936=VERTEX_POINT('',#22738);
#6937=VERTEX_POINT('',#22744);
#6938=VERTEX_POINT('',#22745);
#6939=VERTEX_POINT('',#22749);
#6940=VERTEX_POINT('',#22756);
#6941=VERTEX_POINT('',#22757);
#6942=VERTEX_POINT('',#22761);
#6943=VERTEX_POINT('',#22768);
#6944=VERTEX_POINT('',#22769);
#6945=VERTEX_POINT('',#22773);
#6946=VERTEX_POINT('',#22780);
#6947=VERTEX_POINT('',#22781);
#6948=VERTEX_POINT('',#22785);
#6949=VERTEX_POINT('',#22792);
#8510=EDGE_CURVE('',#6929,#6929,#882,.T.);
#8511=EDGE_CURVE('',#6929,#6930,#4140,.T.);
#8512=EDGE_CURVE('',#6930,#6930,#883,.T.);
#8513=EDGE_CURVE('',#6931,#6931,#884,.T.);
#8514=EDGE_CURVE('',#6931,#6929,#4141,.T.);
#8515=EDGE_CURVE('',#6932,#6933,#408,.T.);
#8516=EDGE_CURVE('',#6934,#6932,#4142,.T.);
#8517=EDGE_CURVE('',#6935,#6934,#4143,.T.);
#8518=EDGE_CURVE('',#6935,#6936,#4144,.T.);
#8519=EDGE_CURVE('',#6933,#6936,#409,.T.);
#8520=EDGE_CURVE('',#6937,#6938,#410,.T.);
#8521=EDGE_CURVE('',#6939,#6937,#4145,.T.);
#8522=EDGE_CURVE('',#6934,#6939,#4146,.T.);
#8523=EDGE_CURVE('',#6938,#6932,#411,.T.);
#8524=EDGE_CURVE('',#6940,#6941,#412,.T.);
#8525=EDGE_CURVE('',#6942,#6940,#4147,.T.);
#8526=EDGE_CURVE('',#6939,#6942,#4148,.T.);
#8527=EDGE_CURVE('',#6941,#6937,#413,.T.);
#8528=EDGE_CURVE('',#6943,#6944,#414,.T.);
#8529=EDGE_CURVE('',#6945,#6943,#4149,.T.);
#8530=EDGE_CURVE('',#6942,#6945,#4150,.T.);
#8531=EDGE_CURVE('',#6944,#6940,#415,.T.);
#8532=EDGE_CURVE('',#6946,#6947,#416,.T.);
#8533=EDGE_CURVE('',#6948,#6946,#4151,.T.);
#8534=EDGE_CURVE('',#6945,#6948,#4152,.T.);
#8535=EDGE_CURVE('',#6947,#6943,#417,.T.);
#8536=EDGE_CURVE('',#6936,#6949,#418,.T.);
#8537=EDGE_CURVE('',#6948,#6935,#4153,.T.);
#8538=EDGE_CURVE('',#6949,#6946,#419,.T.);
#8539=EDGE_CURVE('',#6947,#6949,#885,.T.);
#8540=EDGE_CURVE('',#6944,#6947,#886,.T.);
#8541=EDGE_CURVE('',#6941,#6944,#887,.T.);
#8542=EDGE_CURVE('',#6941,#6938,#888,.T.);
#8543=EDGE_CURVE('',#6933,#6938,#889,.T.);
#8544=EDGE_CURVE('',#6949,#6933,#890,.T.);
#11253=ORIENTED_EDGE('',*,*,#8510,.F.);
#11254=ORIENTED_EDGE('',*,*,#8511,.T.);
#11255=ORIENTED_EDGE('',*,*,#8512,.T.);
#11256=ORIENTED_EDGE('',*,*,#8511,.F.);
#11257=ORIENTED_EDGE('',*,*,#8513,.F.);
#11258=ORIENTED_EDGE('',*,*,#8514,.T.);
#11259=ORIENTED_EDGE('',*,*,#8510,.T.);
#11260=ORIENTED_EDGE('',*,*,#8514,.F.);
#11261=ORIENTED_EDGE('',*,*,#8515,.F.);
#11262=ORIENTED_EDGE('',*,*,#8516,.F.);
#11263=ORIENTED_EDGE('',*,*,#8517,.F.);
#11264=ORIENTED_EDGE('',*,*,#8518,.T.);
#11265=ORIENTED_EDGE('',*,*,#8519,.F.);
#11266=ORIENTED_EDGE('',*,*,#8520,.F.);
#11267=ORIENTED_EDGE('',*,*,#8521,.F.);
#11268=ORIENTED_EDGE('',*,*,#8522,.F.);
#11269=ORIENTED_EDGE('',*,*,#8516,.T.);
#11270=ORIENTED_EDGE('',*,*,#8523,.F.);
#11271=ORIENTED_EDGE('',*,*,#8524,.F.);
#11272=ORIENTED_EDGE('',*,*,#8525,.F.);
#11273=ORIENTED_EDGE('',*,*,#8526,.F.);
#11274=ORIENTED_EDGE('',*,*,#8521,.T.);
#11275=ORIENTED_EDGE('',*,*,#8527,.F.);
#11276=ORIENTED_EDGE('',*,*,#8528,.F.);
#11277=ORIENTED_EDGE('',*,*,#8529,.F.);
#11278=ORIENTED_EDGE('',*,*,#8530,.F.);
#11279=ORIENTED_EDGE('',*,*,#8525,.T.);
#11280=ORIENTED_EDGE('',*,*,#8531,.F.);
#11281=ORIENTED_EDGE('',*,*,#8532,.F.);
#11282=ORIENTED_EDGE('',*,*,#8533,.F.);
#11283=ORIENTED_EDGE('',*,*,#8534,.F.);
#11284=ORIENTED_EDGE('',*,*,#8529,.T.);
#11285=ORIENTED_EDGE('',*,*,#8535,.F.);
#11286=ORIENTED_EDGE('',*,*,#8536,.F.);
#11287=ORIENTED_EDGE('',*,*,#8518,.F.);
#11288=ORIENTED_EDGE('',*,*,#8537,.F.);
#11289=ORIENTED_EDGE('',*,*,#8533,.T.);
#11290=ORIENTED_EDGE('',*,*,#8538,.F.);
#11291=ORIENTED_EDGE('',*,*,#8517,.T.);
#11292=ORIENTED_EDGE('',*,*,#8522,.T.);
#11293=ORIENTED_EDGE('',*,*,#8526,.T.);
#11294=ORIENTED_EDGE('',*,*,#8530,.T.);
#11295=ORIENTED_EDGE('',*,*,#8534,.T.);
#11296=ORIENTED_EDGE('',*,*,#8537,.T.);
#11297=ORIENTED_EDGE('',*,*,#8513,.T.);
#11298=ORIENTED_EDGE('',*,*,#8512,.F.);
#11299=ORIENTED_EDGE('',*,*,#8532,.T.);
#11300=ORIENTED_EDGE('',*,*,#8539,.T.);
#11301=ORIENTED_EDGE('',*,*,#8538,.T.);
#11302=ORIENTED_EDGE('',*,*,#8528,.T.);
#11303=ORIENTED_EDGE('',*,*,#8540,.T.);
#11304=ORIENTED_EDGE('',*,*,#8535,.T.);
#11305=ORIENTED_EDGE('',*,*,#8524,.T.);
#11306=ORIENTED_EDGE('',*,*,#8541,.T.);
#11307=ORIENTED_EDGE('',*,*,#8531,.T.);
#11308=ORIENTED_EDGE('',*,*,#8527,.T.);
#11309=ORIENTED_EDGE('',*,*,#8520,.T.);
#11310=ORIENTED_EDGE('',*,*,#8542,.F.);
#11311=ORIENTED_EDGE('',*,*,#8523,.T.);
#11312=ORIENTED_EDGE('',*,*,#8515,.T.);
#11313=ORIENTED_EDGE('',*,*,#8543,.T.);
#11314=ORIENTED_EDGE('',*,*,#8519,.T.);
#11315=ORIENTED_EDGE('',*,*,#8536,.T.);
#11316=ORIENTED_EDGE('',*,*,#8544,.T.);
#11317=ORIENTED_EDGE('',*,*,#8544,.F.);
#11318=ORIENTED_EDGE('',*,*,#8539,.F.);
#11319=ORIENTED_EDGE('',*,*,#8540,.F.);
#11320=ORIENTED_EDGE('',*,*,#8541,.F.);
#11321=ORIENTED_EDGE('',*,*,#8542,.T.);
#11322=ORIENTED_EDGE('',*,*,#8543,.F.);
#14225=PLANE('',#16282);
#14226=PLANE('',#16283);
#14227=PLANE('',#16284);
#14228=PLANE('',#16285);
#14229=PLANE('',#16286);
#14230=PLANE('',#16287);
#14231=PLANE('',#16288);
#14232=PLANE('',#16289);
#14233=PLANE('',#16302);
#14925=ADVANCED_FACE('',(#1957),#574,.T.);
#14926=ADVANCED_FACE('',(#1958),#1182,.T.);
#14927=ADVANCED_FACE('',(#1959),#14225,.F.);
#14928=ADVANCED_FACE('',(#1960),#14226,.F.);
#14929=ADVANCED_FACE('',(#1961),#14227,.F.);
#14930=ADVANCED_FACE('',(#1962),#14228,.F.);
#14931=ADVANCED_FACE('',(#1963),#14229,.F.);
#14932=ADVANCED_FACE('',(#1964),#14230,.F.);
#14933=ADVANCED_FACE('',(#1965,#1595),#14231,.T.);
#14934=ADVANCED_FACE('',(#1966),#14232,.F.);
#14935=ADVANCED_FACE('',(#1967),#575,.T.);
#14936=ADVANCED_FACE('',(#1968),#576,.T.);
#14937=ADVANCED_FACE('',(#1969),#577,.T.);
#14938=ADVANCED_FACE('',(#1970),#578,.T.);
#14939=ADVANCED_FACE('',(#1971),#579,.T.);
#14940=ADVANCED_FACE('',(#1972),#580,.T.);
#14941=ADVANCED_FACE('',(#1973),#14233,.F.);
#15567=CLOSED_SHELL('',(#14925,#14926,#14927,#14928,#14929,#14930,#14931,
#14932,#14933,#14934,#14935,#14936,#14937,#14938,#14939,#14940,#14941));
#16276=AXIS2_PLACEMENT_3D('',#22717,#18610,#18611);
#16277=AXIS2_PLACEMENT_3D('',#22718,#18612,#18613);
#16278=AXIS2_PLACEMENT_3D('',#22720,#18614,#18615);
#16279=AXIS2_PLACEMENT_3D('',#22723,#18617,#18618);
#16280=AXIS2_PLACEMENT_3D('',#22724,#18619,#18620);
#16281=AXIS2_PLACEMENT_3D('',#22726,#18621,#18622);
#16282=AXIS2_PLACEMENT_3D('',#22728,#18624,#18625);
#16283=AXIS2_PLACEMENT_3D('',#22743,#18629,#18630);
#16284=AXIS2_PLACEMENT_3D('',#22755,#18633,#18634);
#16285=AXIS2_PLACEMENT_3D('',#22767,#18637,#18638);
#16286=AXIS2_PLACEMENT_3D('',#22779,#18641,#18642);
#16287=AXIS2_PLACEMENT_3D('',#22791,#18645,#18646);
#16288=AXIS2_PLACEMENT_3D('',#22800,#18648,#18649);
#16289=AXIS2_PLACEMENT_3D('',#22801,#18650,#18651);
#16290=AXIS2_PLACEMENT_3D('',#22802,#18652,#18653);
#16291=AXIS2_PLACEMENT_3D('',#22803,#18654,#18655);
#16292=AXIS2_PLACEMENT_3D('',#22804,#18656,#18657);
#16293=AXIS2_PLACEMENT_3D('',#22805,#18658,#18659);
#16294=AXIS2_PLACEMENT_3D('',#22806,#18660,#18661);
#16295=AXIS2_PLACEMENT_3D('',#22807,#18662,#18663);
#16296=AXIS2_PLACEMENT_3D('',#22808,#18664,#18665);
#16297=AXIS2_PLACEMENT_3D('',#22809,#18666,#18667);
#16298=AXIS2_PLACEMENT_3D('',#22810,#18668,#18669);
#16299=AXIS2_PLACEMENT_3D('',#22811,#18670,#18671);
#16300=AXIS2_PLACEMENT_3D('',#22812,#18672,#18673);
#16301=AXIS2_PLACEMENT_3D('',#22813,#18674,#18675);
#16302=AXIS2_PLACEMENT_3D('',#22814,#18676,#18677);
#18610=DIRECTION('axis',(0.,0.,1.));
#18611=DIRECTION('refdir',(1.,0.,0.));
#18612=DIRECTION('center_axis',(-1.,0.,0.));
#18613=DIRECTION('ref_axis',(0.,0.,1.));
#18614=DIRECTION('center_axis',(-1.,0.,0.));
#18615=DIRECTION('ref_axis',(0.,0.,1.));
#18616=DIRECTION('',(0.707106781186548,8.65956056235493E-17,0.707106781186547));
#18617=DIRECTION('center_axis',(-1.,0.,0.));
#18618=DIRECTION('ref_axis',(0.,0.,1.));
#18619=DIRECTION('center_axis',(-1.,0.,0.));
#18620=DIRECTION('ref_axis',(0.,0.,1.));
#18621=DIRECTION('center_axis',(-1.,0.,0.));
#18622=DIRECTION('ref_axis',(0.,0.,-1.));
#18623=DIRECTION('',(1.,0.,0.));
#18624=DIRECTION('center_axis',(0.,-0.866025403784438,0.500000000000001));
#18625=DIRECTION('ref_axis',(0.,-0.500000000000001,-0.866025403784438));
#18626=DIRECTION('',(-1.,0.,0.));
#18627=DIRECTION('',(0.,0.500000000000001,0.866025403784438));
#18628=DIRECTION('',(-1.,0.,0.));
#18629=DIRECTION('center_axis',(0.,-0.866025403784438,-0.500000000000001));
#18630=DIRECTION('ref_axis',(0.,0.500000000000001,-0.866025403784438));
#18631=DIRECTION('',(-1.,0.,0.));
#18632=DIRECTION('',(0.,-0.500000000000001,0.866025403784438));
#18633=DIRECTION('center_axis',(0.,-1.11386523624802E-16,-1.));
#18634=DIRECTION('ref_axis',(0.,1.,-1.11386523624802E-16));
#18635=DIRECTION('',(-1.,0.,0.));
#18636=DIRECTION('',(0.,-1.,1.11386523624802E-16));
#18637=DIRECTION('center_axis',(0.,0.866025403784438,-0.500000000000001));
#18638=DIRECTION('ref_axis',(0.,0.500000000000001,0.866025403784438));
#18639=DIRECTION('',(-1.,0.,0.));
#18640=DIRECTION('',(0.,-0.500000000000001,-0.866025403784438));
#18641=DIRECTION('center_axis',(0.,0.866025403784438,0.500000000000001));
#18642=DIRECTION('ref_axis',(0.,-0.500000000000001,0.866025403784438));
#18643=DIRECTION('',(-1.,0.,0.));
#18644=DIRECTION('',(0.,0.500000000000001,-0.866025403784438));
#18645=DIRECTION('center_axis',(0.,-2.22773047249605E-16,1.));
#18646=DIRECTION('ref_axis',(0.,-1.,-2.22773047249605E-16));
#18647=DIRECTION('',(0.,1.,2.22773047249605E-16));
#18648=DIRECTION('center_axis',(1.,0.,0.));
#18649=DIRECTION('ref_axis',(0.,0.,-1.));
#18650=DIRECTION('center_axis',(-1.,0.,0.));
#18651=DIRECTION('ref_axis',(0.,0.,1.));
#18652=DIRECTION('center_axis',(1.,0.,0.));
#18653=DIRECTION('ref_axis',(0.,0.,-1.));
#18654=DIRECTION('center_axis',(1.,0.,0.));
#18655=DIRECTION('ref_axis',(0.,0.,-1.));
#18656=DIRECTION('center_axis',(1.,0.,0.));
#18657=DIRECTION('ref_axis',(0.,0.,-1.));
#18658=DIRECTION('center_axis',(1.,0.,0.));
#18659=DIRECTION('ref_axis',(0.,0.,-1.));
#18660=DIRECTION('center_axis',(1.,0.,0.));
#18661=DIRECTION('ref_axis',(0.,0.,-1.));
#18662=DIRECTION('center_axis',(1.,0.,0.));
#18663=DIRECTION('ref_axis',(0.,0.,-1.));
#18664=DIRECTION('center_axis',(1.,0.,0.));
#18665=DIRECTION('ref_axis',(0.,0.,-1.));
#18666=DIRECTION('center_axis',(-1.,0.,0.));
#18667=DIRECTION('ref_axis',(0.,0.,1.));
#18668=DIRECTION('center_axis',(1.,0.,0.));
#18669=DIRECTION('ref_axis',(0.,0.,-1.));
#18670=DIRECTION('center_axis',(1.,0.,0.));
#18671=DIRECTION('ref_axis',(0.,0.,-1.));
#18672=DIRECTION('center_axis',(1.,0.,0.));
#18673=DIRECTION('ref_axis',(0.,0.,-1.));
#18674=DIRECTION('center_axis',(1.,0.,0.));
#18675=DIRECTION('ref_axis',(0.,0.,-1.));
#18676=DIRECTION('center_axis',(1.,0.,0.));
#18677=DIRECTION('ref_axis',(0.,0.,-1.));
#22717=CARTESIAN_POINT('',(0.,0.,0.));
#22718=CARTESIAN_POINT('Origin',(55.7276,0.,0.));
#22719=CARTESIAN_POINT('',(54.88813,-9.72063396823211E-16,-7.9375));
#22720=CARTESIAN_POINT('Origin',(54.88813,0.,0.));
#22721=CARTESIAN_POINT('',(55.7276,-8.69257971975189E-16,-7.09803));
#22722=CARTESIAN_POINT('',(55.7276,-8.69257971975189E-16,-7.09803));
#22723=CARTESIAN_POINT('Origin',(55.7276,0.,0.));
#22724=CARTESIAN_POINT('Origin',(0.,0.,0.));
#22725=CARTESIAN_POINT('',(11.2776,-9.72063396823212E-16,-7.9375));
#22726=CARTESIAN_POINT('Origin',(11.2776,0.,0.));
#22727=CARTESIAN_POINT('',(0.,-9.72063396823212E-16,-7.9375));
#22728=CARTESIAN_POINT('Origin',(11.2776,7.78695402066815,-13.4874));
#22729=CARTESIAN_POINT('',(1.20464597933184,15.5739080413363,-7.15323062778294E-16));
#22730=CARTESIAN_POINT('',(0.,11.6804310310022,-6.74370000000001));
#22731=CARTESIAN_POINT('Ctrl Pts',(1.20464597933472,15.5739080413413,8.62256231748444E-12));
#22732=CARTESIAN_POINT('Ctrl Pts',(5.88418203051333E-15,13.487400000002,
-3.61393793799207));
#22733=CARTESIAN_POINT('Ctrl Pts',(5.21480900164849E-15,11.6804310310022,
-6.74370000000001));
#22734=CARTESIAN_POINT('',(11.2776,15.5739080413363,0.));
#22735=CARTESIAN_POINT('',(11.2776,15.5739080413363,0.));
#22736=CARTESIAN_POINT('',(11.2776,7.78695402066815,-13.4874));
#22737=CARTESIAN_POINT('',(11.2776,7.78695402066815,-13.4874));
#22738=CARTESIAN_POINT('',(1.20464597933183,7.78695402066815,-13.4874));
#22739=CARTESIAN_POINT('',(11.2776,7.78695402066815,-13.4874));
#22740=CARTESIAN_POINT('Ctrl Pts',(5.21480900164849E-15,11.6804310310022,
-6.74370000000001));
#22741=CARTESIAN_POINT('Ctrl Pts',(4.72325692176463E-15,9.87346206200247,
-9.87346206200795));
#22742=CARTESIAN_POINT('Ctrl Pts',(1.20464597933471,7.78695402066317,-13.4874000000086));
#22743=CARTESIAN_POINT('Origin',(11.2776,15.5739080413363,0.));
#22744=CARTESIAN_POINT('',(1.20464597933183,7.78695402066815,13.4874));
#22745=CARTESIAN_POINT('',(0.,11.6804310310022,6.74370000000002));
#22746=CARTESIAN_POINT('Ctrl Pts',(1.2046459793347,7.78695402066317,13.4874000000086));
#22747=CARTESIAN_POINT('Ctrl Pts',(4.44089209850063E-16,9.87346206200247,
9.87346206200795));
#22748=CARTESIAN_POINT('Ctrl Pts',(2.75695286792984E-32,11.6804310310022,
6.74370000000002));
#22749=CARTESIAN_POINT('',(11.2776,7.78695402066815,13.4874));
#22750=CARTESIAN_POINT('',(11.2776,7.78695402066815,13.4874));
#22751=CARTESIAN_POINT('',(11.2776,15.5739080413363,0.));
#22752=CARTESIAN_POINT('Ctrl Pts',(2.75695286792984E-32,11.6804310310022,
6.74370000000002));
#22753=CARTESIAN_POINT('Ctrl Pts',(1.64432633682228E-32,13.487400000002,
3.61393793799206));
#22754=CARTESIAN_POINT('Ctrl Pts',(1.20464597933472,15.5739080413413,-8.63647399109626E-12));
#22755=CARTESIAN_POINT('Origin',(11.2776,7.78695402066815,13.4874));
#22756=CARTESIAN_POINT('',(1.20464597933184,-7.78695402066817,13.4874));
#22757=CARTESIAN_POINT('',(0.,1.50231459873716E-15,13.4874));
#22758=CARTESIAN_POINT('Ctrl Pts',(1.20464597933471,-7.78695402067813,13.4874));
#22759=CARTESIAN_POINT('Ctrl Pts',(-2.88657986402541E-15,-3.61393793799953,
13.4874));
#22760=CARTESIAN_POINT('Ctrl Pts',(-3.47653933443233E-15,-1.9865939053899E-15,
13.4874));
#22761=CARTESIAN_POINT('',(11.2776,-7.78695402066817,13.4874));
#22762=CARTESIAN_POINT('',(11.2776,-7.78695402066817,13.4874));
#22763=CARTESIAN_POINT('',(11.2776,7.78695402066815,13.4874));
#22764=CARTESIAN_POINT('Ctrl Pts',(-3.47653933443233E-15,-1.9865939053899E-15,
13.4874));
#22765=CARTESIAN_POINT('Ctrl Pts',(-3.86572425055132E-15,3.61393793799952,
13.4874));
#22766=CARTESIAN_POINT('Ctrl Pts',(1.2046459793347,7.7869540206781,13.4874));
#22767=CARTESIAN_POINT('Origin',(11.2776,-15.5739080413363,2.70693809272771E-16));
#22768=CARTESIAN_POINT('',(1.20464597933185,-15.5739080413363,4.81312603749133E-16));
#22769=CARTESIAN_POINT('',(0.,-11.6804310310022,6.74370000000001));
#22770=CARTESIAN_POINT('Ctrl Pts',(1.20464597933473,-15.5739080413413,-8.62951815429035E-12));
#22771=CARTESIAN_POINT('Ctrl Pts',(1.0325074129014E-14,-13.487400000002,
3.61393793799206));
#22772=CARTESIAN_POINT('Ctrl Pts',(8.44302409790707E-15,-11.6804310310023,
6.74370000000001));
#22773=CARTESIAN_POINT('',(11.2776,-15.5739080413363,2.70693809272771E-16));
#22774=CARTESIAN_POINT('',(11.2776,-15.5739080413363,2.70693809272771E-16));
#22775=CARTESIAN_POINT('',(11.2776,-15.5739080413363,2.70693809272771E-16));
#22776=CARTESIAN_POINT('Ctrl Pts',(8.44302409790707E-15,-11.6804310310023,
6.74370000000001));
#22777=CARTESIAN_POINT('Ctrl Pts',(6.29021451463548E-15,-9.87346206200249,
9.87346206200794));
#22778=CARTESIAN_POINT('Ctrl Pts',(1.20464597933471,-7.7869540206632,13.4874000000086));
#22779=CARTESIAN_POINT('Origin',(11.2776,-7.78695402066818,-13.4874));
#22780=CARTESIAN_POINT('',(1.20464597933184,-7.78695402066818,-13.4874));
#22781=CARTESIAN_POINT('',(0.,-11.6804310310022,-6.74370000000001));
#22782=CARTESIAN_POINT('Ctrl Pts',(1.20464597933471,-7.78695402066319,-13.4874000000086));
#22783=CARTESIAN_POINT('Ctrl Pts',(1.48769885299771E-14,-9.87346206200248,
-9.87346206200796));
#22784=CARTESIAN_POINT('Ctrl Pts',(1.24162119086869E-14,-11.6804310310022,
-6.74370000000003));
#22785=CARTESIAN_POINT('',(11.2776,-7.78695402066818,-13.4874));
#22786=CARTESIAN_POINT('',(11.2776,-7.78695402066818,-13.4874));
#22787=CARTESIAN_POINT('',(11.2776,-7.78695402066818,-13.4874));
#22788=CARTESIAN_POINT('Ctrl Pts',(1.24162119086869E-14,-11.6804310310022,
-6.74370000000003));
#22789=CARTESIAN_POINT('Ctrl Pts',(1.02729326886213E-14,-13.487400000002,
-3.61393793799208));
#22790=CARTESIAN_POINT('Ctrl Pts',(1.20464597933472,-15.5739080413413,8.60758051513325E-12));
#22791=CARTESIAN_POINT('Origin',(11.2776,7.78695402066815,-13.4874));
#22792=CARTESIAN_POINT('',(0.,3.00462919747432E-15,-13.4874));
#22793=CARTESIAN_POINT('Ctrl Pts',(1.20464597933471,7.78695402067811,-13.4874));
#22794=CARTESIAN_POINT('Ctrl Pts',(2.66453525910038E-15,3.61393793799952,
-13.4874));
#22795=CARTESIAN_POINT('Ctrl Pts',(2.48324238173738E-15,0.,-13.4874));
#22796=CARTESIAN_POINT('',(11.2776,7.78695402066815,-13.4874));
#22797=CARTESIAN_POINT('Ctrl Pts',(2.48324238173738E-15,0.,-13.4874));
#22798=CARTESIAN_POINT('Ctrl Pts',(2.55640694962002E-15,-3.61393793799953,
-13.4874));
#22799=CARTESIAN_POINT('Ctrl Pts',(1.20464597933471,-7.78695402067813,-13.4874));
#22800=CARTESIAN_POINT('Origin',(11.2776,15.5739080413363,1.3010426069826E-15));
#22801=CARTESIAN_POINT('Origin',(55.7276,0.,0.));
#22802=CARTESIAN_POINT('Origin',(0.,0.,0.));
#22803=CARTESIAN_POINT('Origin',(0.,0.,0.));
#22804=CARTESIAN_POINT('Origin',(0.,0.,0.));
#22805=CARTESIAN_POINT('Origin',(0.,0.,0.));
#22806=CARTESIAN_POINT('Origin',(0.,0.,0.));
#22807=CARTESIAN_POINT('Origin',(0.,0.,0.));
#22808=CARTESIAN_POINT('Origin',(0.,0.,0.));
#22809=CARTESIAN_POINT('Origin',(0.,0.,0.));
#22810=CARTESIAN_POINT('Origin',(0.,0.,0.));
#22811=CARTESIAN_POINT('Origin',(0.,0.,0.));
#22812=CARTESIAN_POINT('Origin',(0.,0.,0.));
#22813=CARTESIAN_POINT('Origin',(0.,0.,0.));
#22814=CARTESIAN_POINT('Origin',(0.,15.5739080413363,1.3010426069826E-15));
#32876=UNCERTAINTY_MEASURE_WITH_UNIT(LENGTH_MEASURE(0.01),#32904,
'DISTANCE_ACCURACY_VALUE',
'Maximum model space distance between geometric entities at asserted c
onnectivities');
#32886=UNCERTAINTY_MEASURE_WITH_UNIT(LENGTH_MEASURE(0.01),#32904,
'DISTANCE_ACCURACY_VALUE',
'Maximum model space distance between geometric entities at asserted c
onnectivities');
#32893=(
GEOMETRIC_REPRESENTATION_CONTEXT(3)
GLOBAL_UNCERTAINTY_ASSIGNED_CONTEXT((#32876))
GLOBAL_UNIT_ASSIGNED_CONTEXT((#32904,#32906,#32907))
REPRESENTATION_CONTEXT('','3D')
);
#32903=(
GEOMETRIC_REPRESENTATION_CONTEXT(3)
GLOBAL_UNCERTAINTY_ASSIGNED_CONTEXT((#32886))
GLOBAL_UNIT_ASSIGNED_CONTEXT((#32904,#32906,#32907))
REPRESENTATION_CONTEXT('','3D')
);
#32904=(
LENGTH_UNIT()
NAMED_UNIT(*)
SI_UNIT(.MILLI.,.METRE.)
);
#32906=(
NAMED_UNIT(*)
PLANE_ANGLE_UNIT()
SI_UNIT($,.RADIAN.)
);
#32907=(
NAMED_UNIT(*)
SI_UNIT($,.STERADIAN.)
SOLID_ANGLE_UNIT()
);
#32914=SHAPE_DEFINITION_REPRESENTATION(#32930,#33018);
#32930=PRODUCT_DEFINITION_SHAPE('',$,#33035);
#33018=SHAPE_REPRESENTATION('',(#16276),#32893);
#33028=PRODUCT_DEFINITION_CONTEXT('part definition',#33078,'design');
#33035=PRODUCT_DEFINITION('Heavy Hex Bolt 0.625-18 x 1.75 x 1.25',
'Heavy Hex Bolt 0.625-18 x 1.75 x 1.25',#33051,#33028);
#33051=PRODUCT_DEFINITION_FORMATION('',$,#33086);
#33078=APPLICATION_CONTEXT(
'Core Data for Automotive Mechanical Design Process');
#33079=PRODUCT_CONTEXT('part definition',#33078,'mechanical');
#33086=PRODUCT('Heavy Hex Bolt 0.625-18 x 1.75 x 1.25',
'Heavy Hex Bolt 0.625-18 x 1.75 x 1.25',$,(#33079));
#33099=PRESENTATION_STYLE_ASSIGNMENT((#33105));
#33105=SURFACE_STYLE_USAGE(.BOTH.,#33111);
#33111=SURFACE_SIDE_STYLE('',(#33117));
#33117=SURFACE_STYLE_FILL_AREA(#33123);
#33123=FILL_AREA_STYLE('Opaque(31,36,43)',(#33129));
#33129=FILL_AREA_STYLE_COLOUR('Opaque(31,36,43)',#33135);
#33135=COLOUR_RGB('Opaque(31,36,43)',0.12156862745098,0.141176470588235,
0.168627450980392);
ENDSEC;
END-ISO-10303-21;
